ISO-10303-21;
HEADER;
/* Generated by software containing ST-Developer
 * from STEP Tools, Inc. (www.steptools.com) 
 */

FILE_DESCRIPTION(
/* description */ ('PAT-082'),
/* implementation_level */ '2;1');

FILE_NAME(
/* name */ 'M5x14 Cap Screw.step',
/* time_stamp */ '2026-10-29T20:16:13-07:00',
/* author */ (''),
/* organization */ (''),
/* preprocessor_version */ 'ST-DEVELOPER v20.2',
/* originating_system */ 'Autodesk Translation Framework v15.17.0.0',
/* authorisation */ '');

FILE_SCHEMA (('AUTOMOTIVE_DESIGN { 1 0 10303 214 3 1 1 }'));
ENDSEC;

DATA;
#10=MECHANICAL_DESIGN_GEOMETRIC_PRESENTATION_REPRESENTATION('',(#257),#8266);
#167=CONICAL_SURFACE('',#5216,0.4,0.785398163397448);
#168=CONICAL_SURFACE('',#5220,0.41,0.785398163397448);
#169=CONICAL_SURFACE('',#5224,0.26,0.463647609000806);
#179=ORIENTED_CLOSED_SHELL('',*,#4597,.F.);
#182=BREP_WITH_VOIDS('Body1',#4598,(#179));
#213=SHAPE_REPRESENTATION_RELATIONSHIP('SRR','None',#8375,#235);
#235=ADVANCED_BREP_SHAPE_REPRESENTATION('',(#182),#8259);
#257=STYLED_ITEM('',(#8544),#182);
#389=FACE_BOUND('',#1146,.T.);
#514=PLANE('',#5204);
#515=PLANE('',#5205);
#516=PLANE('',#5206);
#517=PLANE('',#5207);
#518=PLANE('',#5208);
#519=PLANE('',#5209);
#520=PLANE('',#5210);
#521=PLANE('',#5211);
#522=PLANE('',#5212);
#523=PLANE('',#5214);
#524=PLANE('',#5222);
#755=FACE_OUTER_BOUND('',#1132,.T.);
#756=FACE_OUTER_BOUND('',#1133,.T.);
#757=FACE_OUTER_BOUND('',#1134,.T.);
#758=FACE_OUTER_BOUND('',#1135,.T.);
#759=FACE_OUTER_BOUND('',#1136,.T.);
#760=FACE_OUTER_BOUND('',#1137,.T.);
#761=FACE_OUTER_BOUND('',#1138,.T.);
#762=FACE_OUTER_BOUND('',#1139,.T.);
#763=FACE_OUTER_BOUND('',#1140,.T.);
#764=FACE_OUTER_BOUND('',#1141,.T.);
#765=FACE_OUTER_BOUND('',#1142,.T.);
#766=FACE_OUTER_BOUND('',#1143,.T.);
#767=FACE_OUTER_BOUND('',#1144,.T.);
#768=FACE_OUTER_BOUND('',#1145,.T.);
#769=FACE_OUTER_BOUND('',#1147,.T.);
#770=FACE_OUTER_BOUND('',#1148,.T.);
#1132=EDGE_LOOP('',(#3890,#3891,#3892,#3893));
#1133=EDGE_LOOP('',(#3894,#3895,#3896,#3897));
#1134=EDGE_LOOP('',(#3898,#3899,#3900,#3901));
#1135=EDGE_LOOP('',(#3902,#3903,#3904,#3905));
#1136=EDGE_LOOP('',(#3906,#3907,#3908,#3909));
#1137=EDGE_LOOP('',(#3910,#3911,#3912,#3913));
#1138=EDGE_LOOP('',(#3914,#3915,#3916,#3917,#3918,#3919));
#1139=EDGE_LOOP('',(#3920,#3921,#3922,#3923,#3924,#3925));
#1140=EDGE_LOOP('',(#3926));
#1141=EDGE_LOOP('',(#3927));
#1142=EDGE_LOOP('',(#3928,#3929,#3930,#3931));
#1143=EDGE_LOOP('',(#3932,#3933,#3934,#3935));
#1144=EDGE_LOOP('',(#3936,#3937,#3938,#3939));
#1145=EDGE_LOOP('',(#3940));
#1146=EDGE_LOOP('',(#3941));
#1147=EDGE_LOOP('',(#3942,#3943,#3944,#3945));
#1148=EDGE_LOOP('',(#3946,#3947,#3948,#3949));
#1471=LINE('',#7817,#1826);
#1472=LINE('',#7819,#1827);
#1473=LINE('',#7821,#1828);
#1474=LINE('',#7822,#1829);
#1475=LINE('',#7825,#1830);
#1476=LINE('',#7827,#1831);
#1477=LINE('',#7828,#1832);
#1478=LINE('',#7831,#1833);
#1479=LINE('',#7833,#1834);
#1480=LINE('',#7834,#1835);
#1481=LINE('',#7837,#1836);
#1482=LINE('',#7839,#1837);
#1483=LINE('',#7840,#1838);
#1484=LINE('',#7843,#1839);
#1485=LINE('',#7845,#1840);
#1486=LINE('',#7846,#1841);
#1487=LINE('',#7848,#1842);
#1488=LINE('',#7849,#1843);
#1489=LINE('',#7861,#1844);
#1490=LINE('',#7865,#1845);
#1491=LINE('',#7869,#1846);
#1492=LINE('',#7876,#1847);
#1493=LINE('',#7878,#1848);
#1826=VECTOR('',#6330,1.);
#1827=VECTOR('',#6331,1.);
#1828=VECTOR('',#6332,1.);
#1829=VECTOR('',#6333,1.);
#1830=VECTOR('',#6336,1.);
#1831=VECTOR('',#6337,1.);
#1832=VECTOR('',#6338,1.);
#1833=VECTOR('',#6341,1.);
#1834=VECTOR('',#6342,1.);
#1835=VECTOR('',#6343,1.);
#1836=VECTOR('',#6346,1.);
#1837=VECTOR('',#6347,1.);
#1838=VECTOR('',#6348,1.);
#1839=VECTOR('',#6351,1.);
#1840=VECTOR('',#6352,1.);
#1841=VECTOR('',#6353,1.);
#1842=VECTOR('',#6356,1.);
#1843=VECTOR('',#6357,1.);
#1844=VECTOR('',#6374,0.4);
#1845=VECTOR('',#6379,0.425);
#1846=VECTOR('',#6384,0.41);
#1847=VECTOR('',#6393,0.26);
#1848=VECTOR('',#6396,0.25);
#2099=CIRCLE('',#5213,0.24505);
#2100=CIRCLE('',#5215,0.375);
#2101=CIRCLE('',#5217,0.425);
#2102=CIRCLE('',#5219,0.425);
#2103=CIRCLE('',#5221,0.395);
#2104=CIRCLE('',#5223,0.27);
#2105=CIRCLE('',#5225,0.24505);
#2413=VERTEX_POINT('',#7815);
#2414=VERTEX_POINT('',#7816);
#2415=VERTEX_POINT('',#7818);
#2416=VERTEX_POINT('',#7820);
#2417=VERTEX_POINT('',#7824);
#2418=VERTEX_POINT('',#7826);
#2419=VERTEX_POINT('',#7830);
#2420=VERTEX_POINT('',#7832);
#2421=VERTEX_POINT('',#7836);
#2422=VERTEX_POINT('',#7838);
#2423=VERTEX_POINT('',#7842);
#2424=VERTEX_POINT('',#7844);
#2425=VERTEX_POINT('',#7853);
#2426=VERTEX_POINT('',#7856);
#2427=VERTEX_POINT('',#7859);
#2428=VERTEX_POINT('',#7863);
#2429=VERTEX_POINT('',#7867);
#2430=VERTEX_POINT('',#7871);
#2431=VERTEX_POINT('',#7874);
#2921=EDGE_CURVE('',#2413,#2414,#1471,.T.);
#2922=EDGE_CURVE('',#2414,#2415,#1472,.T.);
#2923=EDGE_CURVE('',#2415,#2416,#1473,.T.);
#2924=EDGE_CURVE('',#2413,#2416,#1474,.T.);
#2925=EDGE_CURVE('',#2414,#2417,#1475,.T.);
#2926=EDGE_CURVE('',#2417,#2418,#1476,.T.);
#2927=EDGE_CURVE('',#2418,#2415,#1477,.T.);
#2928=EDGE_CURVE('',#2417,#2419,#1478,.T.);
#2929=EDGE_CURVE('',#2419,#2420,#1479,.T.);
#2930=EDGE_CURVE('',#2420,#2418,#1480,.T.);
#2931=EDGE_CURVE('',#2419,#2421,#1481,.T.);
#2932=EDGE_CURVE('',#2421,#2422,#1482,.T.);
#2933=EDGE_CURVE('',#2422,#2420,#1483,.T.);
#2934=EDGE_CURVE('',#2421,#2423,#1484,.T.);
#2935=EDGE_CURVE('',#2423,#2424,#1485,.T.);
#2936=EDGE_CURVE('',#2424,#2422,#1486,.T.);
#2937=EDGE_CURVE('',#2423,#2413,#1487,.T.);
#2938=EDGE_CURVE('',#2416,#2424,#1488,.T.);
#2939=EDGE_CURVE('',#2425,#2425,#2099,.T.);
#2940=EDGE_CURVE('',#2426,#2426,#2100,.T.);
#2941=EDGE_CURVE('',#2427,#2427,#2101,.T.);
#2942=EDGE_CURVE('',#2427,#2426,#1489,.T.);
#2943=EDGE_CURVE('',#2428,#2428,#2102,.T.);
#2944=EDGE_CURVE('',#2428,#2427,#1490,.T.);
#2945=EDGE_CURVE('',#2429,#2429,#2103,.T.);
#2946=EDGE_CURVE('',#2429,#2428,#1491,.T.);
#2947=EDGE_CURVE('',#2430,#2430,#2104,.T.);
#2948=EDGE_CURVE('',#2431,#2431,#2105,.F.);
#2949=EDGE_CURVE('',#2431,#2430,#1492,.T.);
#2950=EDGE_CURVE('',#2425,#2431,#1493,.T.);
#3890=ORIENTED_EDGE('',*,*,#2921,.T.);
#3891=ORIENTED_EDGE('',*,*,#2922,.T.);
#3892=ORIENTED_EDGE('',*,*,#2923,.T.);
#3893=ORIENTED_EDGE('',*,*,#2924,.F.);
#3894=ORIENTED_EDGE('',*,*,#2925,.T.);
#3895=ORIENTED_EDGE('',*,*,#2926,.T.);
#3896=ORIENTED_EDGE('',*,*,#2927,.T.);
#3897=ORIENTED_EDGE('',*,*,#2922,.F.);
#3898=ORIENTED_EDGE('',*,*,#2928,.T.);
#3899=ORIENTED_EDGE('',*,*,#2929,.T.);
#3900=ORIENTED_EDGE('',*,*,#2930,.T.);
#3901=ORIENTED_EDGE('',*,*,#2926,.F.);
#3902=ORIENTED_EDGE('',*,*,#2931,.T.);
#3903=ORIENTED_EDGE('',*,*,#2932,.T.);
#3904=ORIENTED_EDGE('',*,*,#2933,.T.);
#3905=ORIENTED_EDGE('',*,*,#2929,.F.);
#3906=ORIENTED_EDGE('',*,*,#2934,.T.);
#3907=ORIENTED_EDGE('',*,*,#2935,.T.);
#3908=ORIENTED_EDGE('',*,*,#2936,.T.);
#3909=ORIENTED_EDGE('',*,*,#2932,.F.);
#3910=ORIENTED_EDGE('',*,*,#2937,.T.);
#3911=ORIENTED_EDGE('',*,*,#2924,.T.);
#3912=ORIENTED_EDGE('',*,*,#2938,.T.);
#3913=ORIENTED_EDGE('',*,*,#2935,.F.);
#3914=ORIENTED_EDGE('',*,*,#2937,.F.);
#3915=ORIENTED_EDGE('',*,*,#2934,.F.);
#3916=ORIENTED_EDGE('',*,*,#2931,.F.);
#3917=ORIENTED_EDGE('',*,*,#2928,.F.);
#3918=ORIENTED_EDGE('',*,*,#2925,.F.);
#3919=ORIENTED_EDGE('',*,*,#2921,.F.);
#3920=ORIENTED_EDGE('',*,*,#2938,.F.);
#3921=ORIENTED_EDGE('',*,*,#2923,.F.);
#3922=ORIENTED_EDGE('',*,*,#2927,.F.);
#3923=ORIENTED_EDGE('',*,*,#2930,.F.);
#3924=ORIENTED_EDGE('',*,*,#2933,.F.);
#3925=ORIENTED_EDGE('',*,*,#2936,.F.);
#3926=ORIENTED_EDGE('',*,*,#2939,.F.);
#3927=ORIENTED_EDGE('',*,*,#2940,.F.);
#3928=ORIENTED_EDGE('',*,*,#2941,.F.);
#3929=ORIENTED_EDGE('',*,*,#2942,.T.);
#3930=ORIENTED_EDGE('',*,*,#2940,.T.);
#3931=ORIENTED_EDGE('',*,*,#2942,.F.);
#3932=ORIENTED_EDGE('',*,*,#2943,.F.);
#3933=ORIENTED_EDGE('',*,*,#2944,.T.);
#3934=ORIENTED_EDGE('',*,*,#2941,.T.);
#3935=ORIENTED_EDGE('',*,*,#2944,.F.);
#3936=ORIENTED_EDGE('',*,*,#2945,.F.);
#3937=ORIENTED_EDGE('',*,*,#2946,.T.);
#3938=ORIENTED_EDGE('',*,*,#2943,.T.);
#3939=ORIENTED_EDGE('',*,*,#2946,.F.);
#3940=ORIENTED_EDGE('',*,*,#2945,.T.);
#3941=ORIENTED_EDGE('',*,*,#2947,.F.);
#3942=ORIENTED_EDGE('',*,*,#2948,.F.);
#3943=ORIENTED_EDGE('',*,*,#2949,.T.);
#3944=ORIENTED_EDGE('',*,*,#2947,.T.);
#3945=ORIENTED_EDGE('',*,*,#2949,.F.);
#3946=ORIENTED_EDGE('',*,*,#2939,.T.);
#3947=ORIENTED_EDGE('',*,*,#2950,.T.);
#3948=ORIENTED_EDGE('',*,*,#2948,.T.);
#3949=ORIENTED_EDGE('',*,*,#2950,.F.);
#4294=CYLINDRICAL_SURFACE('',#5218,0.425);
#4295=CYLINDRICAL_SURFACE('',#5226,0.24505);
#4494=ADVANCED_FACE('',(#755),#514,.F.);
#4495=ADVANCED_FACE('',(#756),#515,.F.);
#4496=ADVANCED_FACE('',(#757),#516,.F.);
#4497=ADVANCED_FACE('',(#758),#517,.F.);
#4498=ADVANCED_FACE('',(#759),#518,.F.);
#4499=ADVANCED_FACE('',(#760),#519,.F.);
#4500=ADVANCED_FACE('',(#761),#520,.F.);
#4501=ADVANCED_FACE('',(#762),#521,.F.);
#4502=ADVANCED_FACE('',(#763),#522,.F.);
#4503=ADVANCED_FACE('',(#764),#523,.T.);
#4504=ADVANCED_FACE('',(#765),#167,.T.);
#4505=ADVANCED_FACE('',(#766),#4294,.T.);
#4506=ADVANCED_FACE('',(#767),#168,.T.);
#4507=ADVANCED_FACE('',(#768,#389),#524,.T.);
#4508=ADVANCED_FACE('',(#769),#169,.T.);
#4509=ADVANCED_FACE('',(#770),#4295,.T.);
#4597=CLOSED_SHELL('',(#4494,#4495,#4496,#4497,#4498,#4499,#4500,#4501));
#4598=CLOSED_SHELL('',(#4502,#4503,#4504,#4505,#4506,#4507,#4508,#4509));
#5203=AXIS2_PLACEMENT_3D('',#7813,#6326,#6327);
#5204=AXIS2_PLACEMENT_3D('',#7814,#6328,#6329);
#5205=AXIS2_PLACEMENT_3D('',#7823,#6334,#6335);
#5206=AXIS2_PLACEMENT_3D('',#7829,#6339,#6340);
#5207=AXIS2_PLACEMENT_3D('',#7835,#6344,#6345);
#5208=AXIS2_PLACEMENT_3D('',#7841,#6349,#6350);
#5209=AXIS2_PLACEMENT_3D('',#7847,#6354,#6355);
#5210=AXIS2_PLACEMENT_3D('',#7850,#6358,#6359);
#5211=AXIS2_PLACEMENT_3D('',#7851,#6360,#6361);
#5212=AXIS2_PLACEMENT_3D('',#7852,#6362,#6363);
#5213=AXIS2_PLACEMENT_3D('',#7854,#6364,#6365);
#5214=AXIS2_PLACEMENT_3D('',#7855,#6366,#6367);
#5215=AXIS2_PLACEMENT_3D('',#7857,#6368,#6369);
#5216=AXIS2_PLACEMENT_3D('',#7858,#6370,#6371);
#5217=AXIS2_PLACEMENT_3D('',#7860,#6372,#6373);
#5218=AXIS2_PLACEMENT_3D('',#7862,#6375,#6376);
#5219=AXIS2_PLACEMENT_3D('',#7864,#6377,#6378);
#5220=AXIS2_PLACEMENT_3D('',#7866,#6380,#6381);
#5221=AXIS2_PLACEMENT_3D('',#7868,#6382,#6383);
#5222=AXIS2_PLACEMENT_3D('',#7870,#6385,#6386);
#5223=AXIS2_PLACEMENT_3D('',#7872,#6387,#6388);
#5224=AXIS2_PLACEMENT_3D('',#7873,#6389,#6390);
#5225=AXIS2_PLACEMENT_3D('',#7875,#6391,#6392);
#5226=AXIS2_PLACEMENT_3D('',#7877,#6394,#6395);
#6326=DIRECTION('axis',(0.,0.,1.));
#6327=DIRECTION('refdir',(1.,0.,0.));
#6328=DIRECTION('center_axis',(0.866025403784439,0.,-0.5));
#6329=DIRECTION('ref_axis',(0.5,0.,0.866025403784439));
#6330=DIRECTION('',(-0.5,0.,-0.866025403784439));
#6331=DIRECTION('',(0.,-1.,0.));
#6332=DIRECTION('',(0.5,0.,0.866025403784439));
#6333=DIRECTION('',(0.,-1.,0.));
#6334=DIRECTION('center_axis',(1.20185167898973E-16,0.,-1.));
#6335=DIRECTION('ref_axis',(1.,0.,1.20185167898973E-16));
#6336=DIRECTION('',(-1.,0.,-1.20185167898973E-16));
#6337=DIRECTION('',(0.,-1.,0.));
#6338=DIRECTION('',(1.,0.,1.20185167898973E-16));
#6339=DIRECTION('center_axis',(-0.866025403784439,0.,-0.5));
#6340=DIRECTION('ref_axis',(0.5,0.,-0.866025403784439));
#6341=DIRECTION('',(-0.5,0.,0.866025403784439));
#6342=DIRECTION('',(0.,-1.,0.));
#6343=DIRECTION('',(0.5,0.,-0.866025403784439));
#6344=DIRECTION('center_axis',(-0.866025403784439,0.,0.5));
#6345=DIRECTION('ref_axis',(-0.5,0.,-0.866025403784439));
#6346=DIRECTION('',(0.5,0.,0.866025403784439));
#6347=DIRECTION('',(0.,-1.,0.));
#6348=DIRECTION('',(-0.5,0.,-0.866025403784439));
#6349=DIRECTION('center_axis',(-2.40370335797945E-16,0.,1.));
#6350=DIRECTION('ref_axis',(-1.,0.,-2.40370335797945E-16));
#6351=DIRECTION('',(1.,0.,2.40370335797945E-16));
#6352=DIRECTION('',(0.,-1.,0.));
#6353=DIRECTION('',(-1.,0.,-2.40370335797945E-16));
#6354=DIRECTION('center_axis',(0.866025403784439,0.,0.5));
#6355=DIRECTION('ref_axis',(-0.5,0.,0.866025403784439));
#6356=DIRECTION('',(0.5,0.,-0.866025403784439));
#6357=DIRECTION('',(-0.5,0.,0.866025403784439));
#6358=DIRECTION('center_axis',(0.,1.,0.));
#6359=DIRECTION('ref_axis',(1.,0.,0.));
#6360=DIRECTION('center_axis',(0.,-1.,0.));
#6361=DIRECTION('ref_axis',(0.,0.,-1.));
#6362=DIRECTION('center_axis',(0.,1.,0.));
#6363=DIRECTION('ref_axis',(1.,0.,0.));
#6364=DIRECTION('center_axis',(0.,1.,0.));
#6365=DIRECTION('ref_axis',(1.,0.,0.));
#6366=DIRECTION('center_axis',(0.,1.,0.));
#6367=DIRECTION('ref_axis',(0.,0.,1.));
#6368=DIRECTION('center_axis',(0.,-1.,0.));
#6369=DIRECTION('ref_axis',(1.,0.,0.));
#6370=DIRECTION('center_axis',(0.,-1.,0.));
#6371=DIRECTION('ref_axis',(1.,0.,0.));
#6372=DIRECTION('center_axis',(0.,-1.,0.));
#6373=DIRECTION('ref_axis',(1.,0.,0.));
#6374=DIRECTION('',(0.707106781186548,0.707106781186547,8.65956056235493E-17));
#6375=DIRECTION('center_axis',(0.,-1.,0.));
#6376=DIRECTION('ref_axis',(1.,0.,0.));
#6377=DIRECTION('center_axis',(0.,-1.,0.));
#6378=DIRECTION('ref_axis',(1.,0.,0.));
#6379=DIRECTION('',(0.,1.,0.));
#6380=DIRECTION('center_axis',(0.,1.,0.));
#6381=DIRECTION('ref_axis',(1.,0.,0.));
#6382=DIRECTION('center_axis',(0.,-1.,0.));
#6383=DIRECTION('ref_axis',(1.,0.,0.));
#6384=DIRECTION('',(-0.707106781186547,0.707106781186548,-8.65956056235493E-17));
#6385=DIRECTION('center_axis',(0.,-1.,0.));
#6386=DIRECTION('ref_axis',(0.,0.,-1.));
#6387=DIRECTION('center_axis',(0.,-1.,0.));
#6388=DIRECTION('ref_axis',(1.,0.,0.));
#6389=DIRECTION('center_axis',(0.,1.,0.));
#6390=DIRECTION('ref_axis',(1.,0.,0.));
#6391=DIRECTION('center_axis',(0.,1.,0.));
#6392=DIRECTION('ref_axis',(1.,0.,0.));
#6393=DIRECTION('',(-0.447213595499958,0.894427190999916,-5.47678698264203E-17));
#6394=DIRECTION('center_axis',(0.,-1.,0.));
#6395=DIRECTION('ref_axis',(1.,0.,0.));
#6396=DIRECTION('',(0.,1.,0.));
#7813=CARTESIAN_POINT('',(0.,0.,0.));
#7814=CARTESIAN_POINT('Origin',(0.115470053837925,-0.5,-0.2));
#7815=CARTESIAN_POINT('',(0.23094010767585,-0.5,0.));
#7816=CARTESIAN_POINT('',(0.115470053837925,-0.5,-0.2));
#7817=CARTESIAN_POINT('',(0.23094010767585,-0.5,0.));
#7818=CARTESIAN_POINT('',(0.115470053837925,-0.8,-0.2));
#7819=CARTESIAN_POINT('',(0.115470053837925,-0.5,-0.2));
#7820=CARTESIAN_POINT('',(0.23094010767585,-0.8,0.));
#7821=CARTESIAN_POINT('',(0.23094010767585,-0.8,0.));
#7822=CARTESIAN_POINT('',(0.23094010767585,-0.5,0.));
#7823=CARTESIAN_POINT('Origin',(-0.115470053837925,-0.5,-0.2));
#7824=CARTESIAN_POINT('',(-0.115470053837925,-0.5,-0.2));
#7825=CARTESIAN_POINT('',(0.115470053837925,-0.5,-0.2));
#7826=CARTESIAN_POINT('',(-0.115470053837925,-0.8,-0.2));
#7827=CARTESIAN_POINT('',(-0.115470053837925,-0.5,-0.2));
#7828=CARTESIAN_POINT('',(0.115470053837925,-0.8,-0.2));
#7829=CARTESIAN_POINT('Origin',(-0.23094010767585,-0.5,-2.77555756156289E-17));
#7830=CARTESIAN_POINT('',(-0.23094010767585,-0.5,-2.82820063659975E-17));
#7831=CARTESIAN_POINT('',(-0.115470053837925,-0.5,-0.2));
#7832=CARTESIAN_POINT('',(-0.23094010767585,-0.8,-2.77555756156289E-17));
#7833=CARTESIAN_POINT('',(-0.23094010767585,-0.5,-2.82820063659975E-17));
#7834=CARTESIAN_POINT('',(-0.115470053837925,-0.8,-0.2));
#7835=CARTESIAN_POINT('Origin',(-0.115470053837925,-0.5,0.2));
#7836=CARTESIAN_POINT('',(-0.115470053837925,-0.5,0.2));
#7837=CARTESIAN_POINT('',(-0.23094010767585,-0.5,-2.82820063659975E-17));
#7838=CARTESIAN_POINT('',(-0.115470053837925,-0.8,0.2));
#7839=CARTESIAN_POINT('',(-0.115470053837925,-0.5,0.2));
#7840=CARTESIAN_POINT('',(-0.23094010767585,-0.8,-2.82820063659975E-17));
#7841=CARTESIAN_POINT('Origin',(0.115470053837925,-0.5,0.2));
#7842=CARTESIAN_POINT('',(0.115470053837925,-0.5,0.2));
#7843=CARTESIAN_POINT('',(-0.115470053837925,-0.5,0.2));
#7844=CARTESIAN_POINT('',(0.115470053837925,-0.8,0.2));
#7845=CARTESIAN_POINT('',(0.115470053837925,-0.5,0.2));
#7846=CARTESIAN_POINT('',(-0.115470053837925,-0.8,0.2));
#7847=CARTESIAN_POINT('Origin',(0.23094010767585,-0.5,0.));
#7848=CARTESIAN_POINT('',(0.115470053837925,-0.5,0.2));
#7849=CARTESIAN_POINT('',(0.115470053837925,-0.8,0.2));
#7850=CARTESIAN_POINT('Origin',(0.,-0.5,0.));
#7851=CARTESIAN_POINT('Origin',(0.,-0.8,0.));
#7852=CARTESIAN_POINT('Origin',(0.,-1.4,0.));
#7853=CARTESIAN_POINT('',(-0.24505,-1.4,3.00099698131059E-17));
#7854=CARTESIAN_POINT('Origin',(0.,-1.4,0.));
#7855=CARTESIAN_POINT('Origin',(0.375,0.5,0.));
#7856=CARTESIAN_POINT('',(-0.375,0.5,-4.59242549680257E-17));
#7857=CARTESIAN_POINT('Origin',(0.,0.5,0.));
#7858=CARTESIAN_POINT('Origin',(0.,0.475,0.));
#7859=CARTESIAN_POINT('',(-0.425,0.45,-5.20474889637625E-17));
#7860=CARTESIAN_POINT('Origin',(0.,0.45,0.));
#7861=CARTESIAN_POINT('',(-0.4,0.475,-4.89858719658941E-17));
#7862=CARTESIAN_POINT('Origin',(0.,0.24,0.));
#7863=CARTESIAN_POINT('',(-0.425,0.0299999999999998,-5.20474889637625E-17));
#7864=CARTESIAN_POINT('Origin',(0.,0.0299999999999998,0.));
#7865=CARTESIAN_POINT('',(-0.425,0.24,-5.20474889637625E-17));
#7866=CARTESIAN_POINT('Origin',(0.,0.0150000000000001,0.));
#7867=CARTESIAN_POINT('',(-0.395,4.85722573273506E-17,-4.83735485663204E-17));
#7868=CARTESIAN_POINT('Origin',(0.,0.,0.));
#7869=CARTESIAN_POINT('',(-0.41,0.0150000000000001,-5.02105187650415E-17));
#7870=CARTESIAN_POINT('Origin',(0.27,0.,0.));
#7871=CARTESIAN_POINT('',(-0.27,0.,-3.30654635769785E-17));
#7872=CARTESIAN_POINT('Origin',(0.,0.,0.));
#7873=CARTESIAN_POINT('Origin',(0.,-0.02,0.));
#7874=CARTESIAN_POINT('',(-0.24505,-0.0498999999999999,3.00099698131059E-17));
#7875=CARTESIAN_POINT('Origin',(0.,-0.0498999999999999,0.));
#7876=CARTESIAN_POINT('',(-0.26,-0.02,-3.18408167778312E-17));
#7877=CARTESIAN_POINT('Origin',(0.,-0.995,0.));
#7878=CARTESIAN_POINT('',(-0.24505,-0.995,-3.00099698131059E-17));
#8234=UNCERTAINTY_MEASURE_WITH_UNIT(LENGTH_MEASURE(0.001),#8267,
'DISTANCE_ACCURACY_VALUE',
'Maximum model space distance between geometric entities at asserted c
onnectivities');
#8241=UNCERTAINTY_MEASURE_WITH_UNIT(LENGTH_MEASURE(0.001),#8267,
'DISTANCE_ACCURACY_VALUE',
'Maximum model space distance between geometric entities at asserted c
onnectivities');
#8259=(
GEOMETRIC_REPRESENTATION_CONTEXT(3)
GLOBAL_UNCERTAINTY_ASSIGNED_CONTEXT((#8234))
GLOBAL_UNIT_ASSIGNED_CONTEXT((#8267,#8269,#8270))
REPRESENTATION_CONTEXT('','3D')
);
#8266=(
GEOMETRIC_REPRESENTATION_CONTEXT(3)
GLOBAL_UNCERTAINTY_ASSIGNED_CONTEXT((#8241))
GLOBAL_UNIT_ASSIGNED_CONTEXT((#8267,#8269,#8270))
REPRESENTATION_CONTEXT('','3D')
);
#8267=(
LENGTH_UNIT()
NAMED_UNIT(*)
SI_UNIT(.CENTI.,.METRE.)
);
#8269=(
NAMED_UNIT(*)
PLANE_ANGLE_UNIT()
SI_UNIT($,.RADIAN.)
);
#8270=(
NAMED_UNIT(*)
SI_UNIT($,.STERADIAN.)
SOLID_ANGLE_UNIT()
);
#8288=SHAPE_DEFINITION_REPRESENTATION(#8312,#8375);
#8312=PRODUCT_DEFINITION_SHAPE('',$,#8400);
#8375=SHAPE_REPRESENTATION('',(#5203),#8259);
#8382=PRODUCT_DEFINITION_CONTEXT('part definition',#8456,'design');
#8400=PRODUCT_DEFINITION('M5x14 Cap Screw','M5x14 Cap Screw',
#8424,#8382);
#8424=PRODUCT_DEFINITION_FORMATION('',$,#8475);
#8456=APPLICATION_CONTEXT(
'Core Data for Automotive Mechanical Design Process');
#8457=PRODUCT_CONTEXT('part definition',#8456,'mechanical');
#8475=PRODUCT('M5x14 Cap Screw','M5x14 Cap Screw',
'M5x14 Cap Screw',(#8457));
#8538=COLOUR_RGB('Black',0.12,0.14,0.17);
#8539=FILL_AREA_STYLE_COLOUR('',#8538);
#8540=FILL_AREA_STYLE('',(#8539));
#8541=SURFACE_STYLE_FILL_AREA(#8540);
#8542=SURFACE_SIDE_STYLE('',(#8541));
#8543=SURFACE_STYLE_USAGE(.BOTH.,#8542);
#8544=PRESENTATION_STYLE_ASSIGNMENT((#8543));
ENDSEC;
END-ISO-10303-21;
